ISO-10303-21;
HEADER;
/* Generated by software containing ST-Developer
 * from STEP Tools, Inc. (www.steptools.com) 
 */

FILE_DESCRIPTION(
/* description */ ('Hinged panel with latch'),
/* implementation_level */ '2;1');

FILE_NAME(
/* name */ 'M5x14 Cap Screw.step',
/* time_stamp */ '2026-10-27T20:36:01-07:00',
/* author */ (''),
/* organization */ (''),
/* preprocessor_version */ 'ST-DEVELOPER v20.2',
/* originating_system */ 'Autodesk Translation Framework v15.17.0.0',
/* authorisation */ '');

FILE_SCHEMA (('AUTOMOTIVE_DESIGN { 1 0 10303 214 3 1 1 }'));
ENDSEC;

DATA;
#10=MECHANICAL_DESIGN_GEOMETRIC_PRESENTATION_REPRESENTATION('',(#303),#6743);
#231=ORIENTED_CLOSED_SHELL('',*,#3805,.F.);
#234=BREP_WITH_VOIDS('Body1',#3806,(#231));
#242=CONICAL_SURFACE('',#4153,0.4,0.785398163397448);
#243=CONICAL_SURFACE('',#4157,0.41,0.785398163397448);
#244=CONICAL_SURFACE('',#4161,0.26,0.463647609000806);
#271=SHAPE_REPRESENTATION_RELATIONSHIP('SRR','None',#6846,#287);
#287=ADVANCED_BREP_SHAPE_REPRESENTATION('',(#234),#6732);
#303=STYLED_ITEM('',(#7010),#234);
#345=FACE_BOUND('',#861,.T.);
#451=PLANE('',#4141);
#452=PLANE('',#4142);
#453=PLANE('',#4143);
#454=PLANE('',#4144);
#455=PLANE('',#4145);
#456=PLANE('',#4146);
#457=PLANE('',#4147);
#458=PLANE('',#4148);
#459=PLANE('',#4149);
#460=PLANE('',#4151);
#461=PLANE('',#4159);
#621=FACE_OUTER_BOUND('',#847,.T.);
#622=FACE_OUTER_BOUND('',#848,.T.);
#623=FACE_OUTER_BOUND('',#849,.T.);
#624=FACE_OUTER_BOUND('',#850,.T.);
#625=FACE_OUTER_BOUND('',#851,.T.);
#626=FACE_OUTER_BOUND('',#852,.T.);
#627=FACE_OUTER_BOUND('',#853,.T.);
#628=FACE_OUTER_BOUND('',#854,.T.);
#629=FACE_OUTER_BOUND('',#855,.T.);
#630=FACE_OUTER_BOUND('',#856,.T.);
#631=FACE_OUTER_BOUND('',#857,.T.);
#632=FACE_OUTER_BOUND('',#858,.T.);
#633=FACE_OUTER_BOUND('',#859,.T.);
#634=FACE_OUTER_BOUND('',#860,.T.);
#635=FACE_OUTER_BOUND('',#862,.T.);
#636=FACE_OUTER_BOUND('',#863,.T.);
#847=EDGE_LOOP('',(#3102,#3103,#3104,#3105));
#848=EDGE_LOOP('',(#3106,#3107,#3108,#3109));
#849=EDGE_LOOP('',(#3110,#3111,#3112,#3113));
#850=EDGE_LOOP('',(#3114,#3115,#3116,#3117));
#851=EDGE_LOOP('',(#3118,#3119,#3120,#3121));
#852=EDGE_LOOP('',(#3122,#3123,#3124,#3125));
#853=EDGE_LOOP('',(#3126,#3127,#3128,#3129,#3130,#3131));
#854=EDGE_LOOP('',(#3132,#3133,#3134,#3135,#3136,#3137));
#855=EDGE_LOOP('',(#3138));
#856=EDGE_LOOP('',(#3139));
#857=EDGE_LOOP('',(#3140,#3141,#3142,#3143));
#858=EDGE_LOOP('',(#3144,#3145,#3146,#3147));
#859=EDGE_LOOP('',(#3148,#3149,#3150,#3151));
#860=EDGE_LOOP('',(#3152));
#861=EDGE_LOOP('',(#3153));
#862=EDGE_LOOP('',(#3154,#3155,#3156,#3157));
#863=EDGE_LOOP('',(#3158,#3159,#3160,#3161));
#1193=LINE('',#6117,#1551);
#1194=LINE('',#6119,#1552);
#1195=LINE('',#6121,#1553);
#1196=LINE('',#6122,#1554);
#1197=LINE('',#6125,#1555);
#1198=LINE('',#6127,#1556);
#1199=LINE('',#6128,#1557);
#1200=LINE('',#6131,#1558);
#1201=LINE('',#6133,#1559);
#1202=LINE('',#6134,#1560);
#1203=LINE('',#6137,#1561);
#1204=LINE('',#6139,#1562);
#1205=LINE('',#6140,#1563);
#1206=LINE('',#6143,#1564);
#1207=LINE('',#6145,#1565);
#1208=LINE('',#6146,#1566);
#1209=LINE('',#6148,#1567);
#1210=LINE('',#6149,#1568);
#1211=LINE('',#6161,#1569);
#1212=LINE('',#6165,#1570);
#1213=LINE('',#6169,#1571);
#1214=LINE('',#6176,#1572);
#1215=LINE('',#6178,#1573);
#1551=VECTOR('',#4871,1.);
#1552=VECTOR('',#4872,1.);
#1553=VECTOR('',#4873,1.);
#1554=VECTOR('',#4874,1.);
#1555=VECTOR('',#4877,1.);
#1556=VECTOR('',#4878,1.);
#1557=VECTOR('',#4879,1.);
#1558=VECTOR('',#4882,1.);
#1559=VECTOR('',#4883,1.);
#1560=VECTOR('',#4884,1.);
#1561=VECTOR('',#4887,1.);
#1562=VECTOR('',#4888,1.);
#1563=VECTOR('',#4889,1.);
#1564=VECTOR('',#4892,1.);
#1565=VECTOR('',#4893,1.);
#1566=VECTOR('',#4894,1.);
#1567=VECTOR('',#4897,1.);
#1568=VECTOR('',#4898,1.);
#1569=VECTOR('',#4915,0.4);
#1570=VECTOR('',#4920,0.425);
#1571=VECTOR('',#4925,0.41);
#1572=VECTOR('',#4934,0.26);
#1573=VECTOR('',#4937,0.25);
#1735=CIRCLE('',#4150,0.24505);
#1736=CIRCLE('',#4152,0.375);
#1737=CIRCLE('',#4154,0.425);
#1738=CIRCLE('',#4156,0.425);
#1739=CIRCLE('',#4158,0.395);
#1740=CIRCLE('',#4160,0.27);
#1741=CIRCLE('',#4162,0.24505);
#1961=VERTEX_POINT('',#6115);
#1962=VERTEX_POINT('',#6116);
#1963=VERTEX_POINT('',#6118);
#1964=VERTEX_POINT('',#6120);
#1965=VERTEX_POINT('',#6124);
#1966=VERTEX_POINT('',#6126);
#1967=VERTEX_POINT('',#6130);
#1968=VERTEX_POINT('',#6132);
#1969=VERTEX_POINT('',#6136);
#1970=VERTEX_POINT('',#6138);
#1971=VERTEX_POINT('',#6142);
#1972=VERTEX_POINT('',#6144);
#1973=VERTEX_POINT('',#6153);
#1974=VERTEX_POINT('',#6156);
#1975=VERTEX_POINT('',#6159);
#1976=VERTEX_POINT('',#6163);
#1977=VERTEX_POINT('',#6167);
#1978=VERTEX_POINT('',#6171);
#1979=VERTEX_POINT('',#6174);
#2363=EDGE_CURVE('',#1961,#1962,#1193,.T.);
#2364=EDGE_CURVE('',#1962,#1963,#1194,.T.);
#2365=EDGE_CURVE('',#1963,#1964,#1195,.T.);
#2366=EDGE_CURVE('',#1961,#1964,#1196,.T.);
#2367=EDGE_CURVE('',#1962,#1965,#1197,.T.);
#2368=EDGE_CURVE('',#1965,#1966,#1198,.T.);
#2369=EDGE_CURVE('',#1966,#1963,#1199,.T.);
#2370=EDGE_CURVE('',#1965,#1967,#1200,.T.);
#2371=EDGE_CURVE('',#1967,#1968,#1201,.T.);
#2372=EDGE_CURVE('',#1968,#1966,#1202,.T.);
#2373=EDGE_CURVE('',#1967,#1969,#1203,.T.);
#2374=EDGE_CURVE('',#1969,#1970,#1204,.T.);
#2375=EDGE_CURVE('',#1970,#1968,#1205,.T.);
#2376=EDGE_CURVE('',#1969,#1971,#1206,.T.);
#2377=EDGE_CURVE('',#1971,#1972,#1207,.T.);
#2378=EDGE_CURVE('',#1972,#1970,#1208,.T.);
#2379=EDGE_CURVE('',#1971,#1961,#1209,.T.);
#2380=EDGE_CURVE('',#1964,#1972,#1210,.T.);
#2381=EDGE_CURVE('',#1973,#1973,#1735,.T.);
#2382=EDGE_CURVE('',#1974,#1974,#1736,.T.);
#2383=EDGE_CURVE('',#1975,#1975,#1737,.T.);
#2384=EDGE_CURVE('',#1975,#1974,#1211,.T.);
#2385=EDGE_CURVE('',#1976,#1976,#1738,.T.);
#2386=EDGE_CURVE('',#1976,#1975,#1212,.T.);
#2387=EDGE_CURVE('',#1977,#1977,#1739,.T.);
#2388=EDGE_CURVE('',#1977,#1976,#1213,.T.);
#2389=EDGE_CURVE('',#1978,#1978,#1740,.T.);
#2390=EDGE_CURVE('',#1979,#1979,#1741,.F.);
#2391=EDGE_CURVE('',#1979,#1978,#1214,.T.);
#2392=EDGE_CURVE('',#1973,#1979,#1215,.T.);
#3102=ORIENTED_EDGE('',*,*,#2363,.T.);
#3103=ORIENTED_EDGE('',*,*,#2364,.T.);
#3104=ORIENTED_EDGE('',*,*,#2365,.T.);
#3105=ORIENTED_EDGE('',*,*,#2366,.F.);
#3106=ORIENTED_EDGE('',*,*,#2367,.T.);
#3107=ORIENTED_EDGE('',*,*,#2368,.T.);
#3108=ORIENTED_EDGE('',*,*,#2369,.T.);
#3109=ORIENTED_EDGE('',*,*,#2364,.F.);
#3110=ORIENTED_EDGE('',*,*,#2370,.T.);
#3111=ORIENTED_EDGE('',*,*,#2371,.T.);
#3112=ORIENTED_EDGE('',*,*,#2372,.T.);
#3113=ORIENTED_EDGE('',*,*,#2368,.F.);
#3114=ORIENTED_EDGE('',*,*,#2373,.T.);
#3115=ORIENTED_EDGE('',*,*,#2374,.T.);
#3116=ORIENTED_EDGE('',*,*,#2375,.T.);
#3117=ORIENTED_EDGE('',*,*,#2371,.F.);
#3118=ORIENTED_EDGE('',*,*,#2376,.T.);
#3119=ORIENTED_EDGE('',*,*,#2377,.T.);
#3120=ORIENTED_EDGE('',*,*,#2378,.T.);
#3121=ORIENTED_EDGE('',*,*,#2374,.F.);
#3122=ORIENTED_EDGE('',*,*,#2379,.T.);
#3123=ORIENTED_EDGE('',*,*,#2366,.T.);
#3124=ORIENTED_EDGE('',*,*,#2380,.T.);
#3125=ORIENTED_EDGE('',*,*,#2377,.F.);
#3126=ORIENTED_EDGE('',*,*,#2379,.F.);
#3127=ORIENTED_EDGE('',*,*,#2376,.F.);
#3128=ORIENTED_EDGE('',*,*,#2373,.F.);
#3129=ORIENTED_EDGE('',*,*,#2370,.F.);
#3130=ORIENTED_EDGE('',*,*,#2367,.F.);
#3131=ORIENTED_EDGE('',*,*,#2363,.F.);
#3132=ORIENTED_EDGE('',*,*,#2380,.F.);
#3133=ORIENTED_EDGE('',*,*,#2365,.F.);
#3134=ORIENTED_EDGE('',*,*,#2369,.F.);
#3135=ORIENTED_EDGE('',*,*,#2372,.F.);
#3136=ORIENTED_EDGE('',*,*,#2375,.F.);
#3137=ORIENTED_EDGE('',*,*,#2378,.F.);
#3138=ORIENTED_EDGE('',*,*,#2381,.F.);
#3139=ORIENTED_EDGE('',*,*,#2382,.F.);
#3140=ORIENTED_EDGE('',*,*,#2383,.F.);
#3141=ORIENTED_EDGE('',*,*,#2384,.T.);
#3142=ORIENTED_EDGE('',*,*,#2382,.T.);
#3143=ORIENTED_EDGE('',*,*,#2384,.F.);
#3144=ORIENTED_EDGE('',*,*,#2385,.F.);
#3145=ORIENTED_EDGE('',*,*,#2386,.T.);
#3146=ORIENTED_EDGE('',*,*,#2383,.T.);
#3147=ORIENTED_EDGE('',*,*,#2386,.F.);
#3148=ORIENTED_EDGE('',*,*,#2387,.F.);
#3149=ORIENTED_EDGE('',*,*,#2388,.T.);
#3150=ORIENTED_EDGE('',*,*,#2385,.T.);
#3151=ORIENTED_EDGE('',*,*,#2388,.F.);
#3152=ORIENTED_EDGE('',*,*,#2387,.T.);
#3153=ORIENTED_EDGE('',*,*,#2389,.F.);
#3154=ORIENTED_EDGE('',*,*,#2390,.F.);
#3155=ORIENTED_EDGE('',*,*,#2391,.T.);
#3156=ORIENTED_EDGE('',*,*,#2389,.T.);
#3157=ORIENTED_EDGE('',*,*,#2391,.F.);
#3158=ORIENTED_EDGE('',*,*,#2381,.T.);
#3159=ORIENTED_EDGE('',*,*,#2392,.T.);
#3160=ORIENTED_EDGE('',*,*,#2390,.T.);
#3161=ORIENTED_EDGE('',*,*,#2392,.F.);
#3572=CYLINDRICAL_SURFACE('',#4155,0.425);
#3573=CYLINDRICAL_SURFACE('',#4163,0.24505);
#3690=ADVANCED_FACE('',(#621),#451,.F.);
#3691=ADVANCED_FACE('',(#622),#452,.F.);
#3692=ADVANCED_FACE('',(#623),#453,.F.);
#3693=ADVANCED_FACE('',(#624),#454,.F.);
#3694=ADVANCED_FACE('',(#625),#455,.F.);
#3695=ADVANCED_FACE('',(#626),#456,.F.);
#3696=ADVANCED_FACE('',(#627),#457,.F.);
#3697=ADVANCED_FACE('',(#628),#458,.F.);
#3698=ADVANCED_FACE('',(#629),#459,.F.);
#3699=ADVANCED_FACE('',(#630),#460,.T.);
#3700=ADVANCED_FACE('',(#631),#242,.T.);
#3701=ADVANCED_FACE('',(#632),#3572,.T.);
#3702=ADVANCED_FACE('',(#633),#243,.T.);
#3703=ADVANCED_FACE('',(#634,#345),#461,.T.);
#3704=ADVANCED_FACE('',(#635),#244,.T.);
#3705=ADVANCED_FACE('',(#636),#3573,.T.);
#3805=CLOSED_SHELL('',(#3690,#3691,#3692,#3693,#3694,#3695,#3696,#3697));
#3806=CLOSED_SHELL('',(#3698,#3699,#3700,#3701,#3702,#3703,#3704,#3705));
#4140=AXIS2_PLACEMENT_3D('',#6113,#4867,#4868);
#4141=AXIS2_PLACEMENT_3D('',#6114,#4869,#4870);
#4142=AXIS2_PLACEMENT_3D('',#6123,#4875,#4876);
#4143=AXIS2_PLACEMENT_3D('',#6129,#4880,#4881);
#4144=AXIS2_PLACEMENT_3D('',#6135,#4885,#4886);
#4145=AXIS2_PLACEMENT_3D('',#6141,#4890,#4891);
#4146=AXIS2_PLACEMENT_3D('',#6147,#4895,#4896);
#4147=AXIS2_PLACEMENT_3D('',#6150,#4899,#4900);
#4148=AXIS2_PLACEMENT_3D('',#6151,#4901,#4902);
#4149=AXIS2_PLACEMENT_3D('',#6152,#4903,#4904);
#4150=AXIS2_PLACEMENT_3D('',#6154,#4905,#4906);
#4151=AXIS2_PLACEMENT_3D('',#6155,#4907,#4908);
#4152=AXIS2_PLACEMENT_3D('',#6157,#4909,#4910);
#4153=AXIS2_PLACEMENT_3D('',#6158,#4911,#4912);
#4154=AXIS2_PLACEMENT_3D('',#6160,#4913,#4914);
#4155=AXIS2_PLACEMENT_3D('',#6162,#4916,#4917);
#4156=AXIS2_PLACEMENT_3D('',#6164,#4918,#4919);
#4157=AXIS2_PLACEMENT_3D('',#6166,#4921,#4922);
#4158=AXIS2_PLACEMENT_3D('',#6168,#4923,#4924);
#4159=AXIS2_PLACEMENT_3D('',#6170,#4926,#4927);
#4160=AXIS2_PLACEMENT_3D('',#6172,#4928,#4929);
#4161=AXIS2_PLACEMENT_3D('',#6173,#4930,#4931);
#4162=AXIS2_PLACEMENT_3D('',#6175,#4932,#4933);
#4163=AXIS2_PLACEMENT_3D('',#6177,#4935,#4936);
#4867=DIRECTION('axis',(0.,0.,1.));
#4868=DIRECTION('refdir',(1.,0.,0.));
#4869=DIRECTION('center_axis',(0.866025403784439,0.,-0.5));
#4870=DIRECTION('ref_axis',(0.5,0.,0.866025403784439));
#4871=DIRECTION('',(-0.5,0.,-0.866025403784439));
#4872=DIRECTION('',(0.,-1.,0.));
#4873=DIRECTION('',(0.5,0.,0.866025403784439));
#4874=DIRECTION('',(0.,-1.,0.));
#4875=DIRECTION('center_axis',(1.20185167898973E-16,0.,-1.));
#4876=DIRECTION('ref_axis',(1.,0.,1.20185167898973E-16));
#4877=DIRECTION('',(-1.,0.,-1.20185167898973E-16));
#4878=DIRECTION('',(0.,-1.,0.));
#4879=DIRECTION('',(1.,0.,1.20185167898973E-16));
#4880=DIRECTION('center_axis',(-0.866025403784439,0.,-0.5));
#4881=DIRECTION('ref_axis',(0.5,0.,-0.866025403784439));
#4882=DIRECTION('',(-0.5,0.,0.866025403784439));
#4883=DIRECTION('',(0.,-1.,0.));
#4884=DIRECTION('',(0.5,0.,-0.866025403784439));
#4885=DIRECTION('center_axis',(-0.866025403784439,0.,0.5));
#4886=DIRECTION('ref_axis',(-0.5,0.,-0.866025403784439));
#4887=DIRECTION('',(0.5,0.,0.866025403784439));
#4888=DIRECTION('',(0.,-1.,0.));
#4889=DIRECTION('',(-0.5,0.,-0.866025403784439));
#4890=DIRECTION('center_axis',(-2.40370335797945E-16,0.,1.));
#4891=DIRECTION('ref_axis',(-1.,0.,-2.40370335797945E-16));
#4892=DIRECTION('',(1.,0.,2.40370335797945E-16));
#4893=DIRECTION('',(0.,-1.,0.));
#4894=DIRECTION('',(-1.,0.,-2.40370335797945E-16));
#4895=DIRECTION('center_axis',(0.866025403784439,0.,0.5));
#4896=DIRECTION('ref_axis',(-0.5,0.,0.866025403784439));
#4897=DIRECTION('',(0.5,0.,-0.866025403784439));
#4898=DIRECTION('',(-0.5,0.,0.866025403784439));
#4899=DIRECTION('center_axis',(0.,1.,0.));
#4900=DIRECTION('ref_axis',(1.,0.,0.));
#4901=DIRECTION('center_axis',(0.,-1.,0.));
#4902=DIRECTION('ref_axis',(0.,0.,-1.));
#4903=DIRECTION('center_axis',(0.,1.,0.));
#4904=DIRECTION('ref_axis',(1.,0.,0.));
#4905=DIRECTION('center_axis',(0.,1.,0.));
#4906=DIRECTION('ref_axis',(1.,0.,0.));
#4907=DIRECTION('center_axis',(0.,1.,0.));
#4908=DIRECTION('ref_axis',(0.,0.,1.));
#4909=DIRECTION('center_axis',(0.,-1.,0.));
#4910=DIRECTION('ref_axis',(1.,0.,0.));
#4911=DIRECTION('center_axis',(0.,-1.,0.));
#4912=DIRECTION('ref_axis',(1.,0.,0.));
#4913=DIRECTION('center_axis',(0.,-1.,0.));
#4914=DIRECTION('ref_axis',(1.,0.,0.));
#4915=DIRECTION('',(0.707106781186548,0.707106781186547,8.65956056235493E-17));
#4916=DIRECTION('center_axis',(0.,-1.,0.));
#4917=DIRECTION('ref_axis',(1.,0.,0.));
#4918=DIRECTION('center_axis',(0.,-1.,0.));
#4919=DIRECTION('ref_axis',(1.,0.,0.));
#4920=DIRECTION('',(0.,1.,0.));
#4921=DIRECTION('center_axis',(0.,1.,0.));
#4922=DIRECTION('ref_axis',(1.,0.,0.));
#4923=DIRECTION('center_axis',(0.,-1.,0.));
#4924=DIRECTION('ref_axis',(1.,0.,0.));
#4925=DIRECTION('',(-0.707106781186547,0.707106781186548,-8.65956056235493E-17));
#4926=DIRECTION('center_axis',(0.,-1.,0.));
#4927=DIRECTION('ref_axis',(0.,0.,-1.));
#4928=DIRECTION('center_axis',(0.,-1.,0.));
#4929=DIRECTION('ref_axis',(1.,0.,0.));
#4930=DIRECTION('center_axis',(0.,1.,0.));
#4931=DIRECTION('ref_axis',(1.,0.,0.));
#4932=DIRECTION('center_axis',(0.,1.,0.));
#4933=DIRECTION('ref_axis',(1.,0.,0.));
#4934=DIRECTION('',(-0.447213595499958,0.894427190999916,-5.47678698264203E-17));
#4935=DIRECTION('center_axis',(0.,-1.,0.));
#4936=DIRECTION('ref_axis',(1.,0.,0.));
#4937=DIRECTION('',(0.,1.,0.));
#6113=CARTESIAN_POINT('',(0.,0.,0.));
#6114=CARTESIAN_POINT('Origin',(0.115470053837925,-0.5,-0.2));
#6115=CARTESIAN_POINT('',(0.23094010767585,-0.5,0.));
#6116=CARTESIAN_POINT('',(0.115470053837925,-0.5,-0.2));
#6117=CARTESIAN_POINT('',(0.23094010767585,-0.5,0.));
#6118=CARTESIAN_POINT('',(0.115470053837925,-0.8,-0.2));
#6119=CARTESIAN_POINT('',(0.115470053837925,-0.5,-0.2));
#6120=CARTESIAN_POINT('',(0.23094010767585,-0.8,0.));
#6121=CARTESIAN_POINT('',(0.23094010767585,-0.8,0.));
#6122=CARTESIAN_POINT('',(0.23094010767585,-0.5,0.));
#6123=CARTESIAN_POINT('Origin',(-0.115470053837925,-0.5,-0.2));
#6124=CARTESIAN_POINT('',(-0.115470053837925,-0.5,-0.2));
#6125=CARTESIAN_POINT('',(0.115470053837925,-0.5,-0.2));
#6126=CARTESIAN_POINT('',(-0.115470053837925,-0.8,-0.2));
#6127=CARTESIAN_POINT('',(-0.115470053837925,-0.5,-0.2));
#6128=CARTESIAN_POINT('',(0.115470053837925,-0.8,-0.2));
#6129=CARTESIAN_POINT('Origin',(-0.23094010767585,-0.5,-2.77555756156289E-17));
#6130=CARTESIAN_POINT('',(-0.23094010767585,-0.5,-2.82820063659975E-17));
#6131=CARTESIAN_POINT('',(-0.115470053837925,-0.5,-0.2));
#6132=CARTESIAN_POINT('',(-0.23094010767585,-0.8,-2.77555756156289E-17));
#6133=CARTESIAN_POINT('',(-0.23094010767585,-0.5,-2.82820063659975E-17));
#6134=CARTESIAN_POINT('',(-0.115470053837925,-0.8,-0.2));
#6135=CARTESIAN_POINT('Origin',(-0.115470053837925,-0.5,0.2));
#6136=CARTESIAN_POINT('',(-0.115470053837925,-0.5,0.2));
#6137=CARTESIAN_POINT('',(-0.23094010767585,-0.5,-2.82820063659975E-17));
#6138=CARTESIAN_POINT('',(-0.115470053837925,-0.8,0.2));
#6139=CARTESIAN_POINT('',(-0.115470053837925,-0.5,0.2));
#6140=CARTESIAN_POINT('',(-0.23094010767585,-0.8,-2.82820063659975E-17));
#6141=CARTESIAN_POINT('Origin',(0.115470053837925,-0.5,0.2));
#6142=CARTESIAN_POINT('',(0.115470053837925,-0.5,0.2));
#6143=CARTESIAN_POINT('',(-0.115470053837925,-0.5,0.2));
#6144=CARTESIAN_POINT('',(0.115470053837925,-0.8,0.2));
#6145=CARTESIAN_POINT('',(0.115470053837925,-0.5,0.2));
#6146=CARTESIAN_POINT('',(-0.115470053837925,-0.8,0.2));
#6147=CARTESIAN_POINT('Origin',(0.23094010767585,-0.5,0.));
#6148=CARTESIAN_POINT('',(0.115470053837925,-0.5,0.2));
#6149=CARTESIAN_POINT('',(0.115470053837925,-0.8,0.2));
#6150=CARTESIAN_POINT('Origin',(0.,-0.5,0.));
#6151=CARTESIAN_POINT('Origin',(0.,-0.8,0.));
#6152=CARTESIAN_POINT('Origin',(0.,-1.4,0.));
#6153=CARTESIAN_POINT('',(-0.24505,-1.4,3.00099698131059E-17));
#6154=CARTESIAN_POINT('Origin',(0.,-1.4,0.));
#6155=CARTESIAN_POINT('Origin',(0.375,0.5,0.));
#6156=CARTESIAN_POINT('',(-0.375,0.5,-4.59242549680257E-17));
#6157=CARTESIAN_POINT('Origin',(0.,0.5,0.));
#6158=CARTESIAN_POINT('Origin',(0.,0.475,0.));
#6159=CARTESIAN_POINT('',(-0.425,0.45,-5.20474889637625E-17));
#6160=CARTESIAN_POINT('Origin',(0.,0.45,0.));
#6161=CARTESIAN_POINT('',(-0.4,0.475,-4.89858719658941E-17));
#6162=CARTESIAN_POINT('Origin',(0.,0.24,0.));
#6163=CARTESIAN_POINT('',(-0.425,0.0299999999999998,-5.20474889637625E-17));
#6164=CARTESIAN_POINT('Origin',(0.,0.0299999999999998,0.));
#6165=CARTESIAN_POINT('',(-0.425,0.24,-5.20474889637625E-17));
#6166=CARTESIAN_POINT('Origin',(0.,0.0150000000000001,0.));
#6167=CARTESIAN_POINT('',(-0.395,4.85722573273506E-17,-4.83735485663204E-17));
#6168=CARTESIAN_POINT('Origin',(0.,0.,0.));
#6169=CARTESIAN_POINT('',(-0.41,0.0150000000000001,-5.02105187650415E-17));
#6170=CARTESIAN_POINT('Origin',(0.27,0.,0.));
#6171=CARTESIAN_POINT('',(-0.27,0.,-3.30654635769785E-17));
#6172=CARTESIAN_POINT('Origin',(0.,0.,0.));
#6173=CARTESIAN_POINT('Origin',(0.,-0.02,0.));
#6174=CARTESIAN_POINT('',(-0.24505,-0.0498999999999999,3.00099698131059E-17));
#6175=CARTESIAN_POINT('Origin',(0.,-0.0498999999999999,0.));
#6176=CARTESIAN_POINT('',(-0.26,-0.02,-3.18408167778312E-17));
#6177=CARTESIAN_POINT('Origin',(0.,-0.995,0.));
#6178=CARTESIAN_POINT('',(-0.24505,-0.995,-3.00099698131059E-17));
#6711=UNCERTAINTY_MEASURE_WITH_UNIT(LENGTH_MEASURE(0.001),#6744,
'DISTANCE_ACCURACY_VALUE',
'Maximum model space distance between geometric entities at asserted c
onnectivities');
#6722=UNCERTAINTY_MEASURE_WITH_UNIT(LENGTH_MEASURE(0.001),#6744,
'DISTANCE_ACCURACY_VALUE',
'Maximum model space distance between geometric entities at asserted c
onnectivities');
#6732=(
GEOMETRIC_REPRESENTATION_CONTEXT(3)
GLOBAL_UNCERTAINTY_ASSIGNED_CONTEXT((#6711))
GLOBAL_UNIT_ASSIGNED_CONTEXT((#6744,#6746,#6747))
REPRESENTATION_CONTEXT('','3D')
);
#6743=(
GEOMETRIC_REPRESENTATION_CONTEXT(3)
GLOBAL_UNCERTAINTY_ASSIGNED_CONTEXT((#6722))
GLOBAL_UNIT_ASSIGNED_CONTEXT((#6744,#6746,#6747))
REPRESENTATION_CONTEXT('','3D')
);
#6744=(
LENGTH_UNIT()
NAMED_UNIT(*)
SI_UNIT(.CENTI.,.METRE.)
);
#6746=(
NAMED_UNIT(*)
PLANE_ANGLE_UNIT()
SI_UNIT($,.RADIAN.)
);
#6747=(
NAMED_UNIT(*)
SI_UNIT($,.STERADIAN.)
SOLID_ANGLE_UNIT()
);
#6757=SHAPE_DEFINITION_REPRESENTATION(#6777,#6846);
#6777=PRODUCT_DEFINITION_SHAPE('',$,#6867);
#6846=SHAPE_REPRESENTATION('',(#4140),#6732);
#6857=PRODUCT_DEFINITION_CONTEXT('part definition',#6919,'design');
#6867=PRODUCT_DEFINITION('M5x14 Cap Screw','M5x14 Cap Screw',#6887,#6857);
#6887=PRODUCT_DEFINITION_FORMATION('',$,#6930);
#6919=APPLICATION_CONTEXT(
'Core Data for Automotive Mechanical Design Process');
#6920=PRODUCT_CONTEXT('part definition',#6919,'mechanical');
#6930=PRODUCT('M5x14 Cap Screw','M5x14 Cap Screw','M5x14 Cap Screw',(#6920));
#7004=COLOUR_RGB('Black',0.12,0.14,0.17);
#7005=FILL_AREA_STYLE_COLOUR('',#7004);
#7006=FILL_AREA_STYLE('',(#7005));
#7007=SURFACE_STYLE_FILL_AREA(#7006);
#7008=SURFACE_SIDE_STYLE('',(#7007));
#7009=SURFACE_STYLE_USAGE(.BOTH.,#7008);
#7010=PRESENTATION_STYLE_ASSIGNMENT((#7009));
ENDSEC;
END-ISO-10303-21;
